ISO-10303-21;
HEADER;
/* Generated by software containing ST-Developer
 * from STEP Tools, Inc. (www.steptools.com) 
 */

FILE_DESCRIPTION(
/* description */ ('Fatigue rig crank-slider'),
/* implementation_level */ '2;1');

FILE_NAME(
/* name */ 'M8x25 Bolt.step',
/* time_stamp */ '2026-10-28T03:24:50-07:00',
/* author */ (''),
/* organization */ (''),
/* preprocessor_version */ 'ST-DEVELOPER v20.2',
/* originating_system */ 'Autodesk Translation Framework v15.17.0.0',
/* authorisation */ '');

FILE_SCHEMA (('AUTOMOTIVE_DESIGN { 1 0 10303 214 3 1 1 }'));
ENDSEC;

DATA;
#10=MECHANICAL_DESIGN_GEOMETRIC_PRESENTATION_REPRESENTATION('',(#601),#16911);
#13=CONICAL_SURFACE('',#9819,0.625,0.785398163397448);
#14=CONICAL_SURFACE('',#9823,0.635,0.785398163397449);
#15=CONICAL_SURFACE('',#9827,0.41,0.463647609000806);
#37=ORIENTED_CLOSED_SHELL('',*,#8892,.F.);
#42=BREP_WITH_VOIDS('Body1',#8893,(#37));
#500=SHAPE_REPRESENTATION_RELATIONSHIP('SRR','None',#17140,#550);
#550=ADVANCED_BREP_SHAPE_REPRESENTATION('',(#42),#16869);
#601=STYLED_ITEM('',(#17494),#42);
#807=FACE_BOUND('',#2022,.T.);
#987=PLANE('',#9807);
#988=PLANE('',#9808);
#989=PLANE('',#9809);
#990=PLANE('',#9810);
#991=PLANE('',#9811);
#992=PLANE('',#9812);
#993=PLANE('',#9813);
#994=PLANE('',#9814);
#995=PLANE('',#9815);
#996=PLANE('',#9817);
#997=PLANE('',#9825);
#1378=FACE_OUTER_BOUND('',#2008,.T.);
#1379=FACE_OUTER_BOUND('',#2009,.T.);
#1380=FACE_OUTER_BOUND('',#2010,.T.);
#1381=FACE_OUTER_BOUND('',#2011,.T.);
#1382=FACE_OUTER_BOUND('',#2012,.T.);
#1383=FACE_OUTER_BOUND('',#2013,.T.);
#1384=FACE_OUTER_BOUND('',#2014,.T.);
#1385=FACE_OUTER_BOUND('',#2015,.T.);
#1386=FACE_OUTER_BOUND('',#2016,.T.);
#1387=FACE_OUTER_BOUND('',#2017,.T.);
#1388=FACE_OUTER_BOUND('',#2018,.T.);
#1389=FACE_OUTER_BOUND('',#2019,.T.);
#1390=FACE_OUTER_BOUND('',#2020,.T.);
#1391=FACE_OUTER_BOUND('',#2021,.T.);
#1392=FACE_OUTER_BOUND('',#2023,.T.);
#1393=FACE_OUTER_BOUND('',#2024,.T.);
#2008=EDGE_LOOP('',(#6676,#6677,#6678,#6679));
#2009=EDGE_LOOP('',(#6680,#6681,#6682,#6683));
#2010=EDGE_LOOP('',(#6684,#6685,#6686,#6687));
#2011=EDGE_LOOP('',(#6688,#6689,#6690,#6691));
#2012=EDGE_LOOP('',(#6692,#6693,#6694,#6695));
#2013=EDGE_LOOP('',(#6696,#6697,#6698,#6699));
#2014=EDGE_LOOP('',(#6700,#6701,#6702,#6703,#6704,#6705));
#2015=EDGE_LOOP('',(#6706,#6707,#6708,#6709,#6710,#6711));
#2016=EDGE_LOOP('',(#6712));
#2017=EDGE_LOOP('',(#6713));
#2018=EDGE_LOOP('',(#6714,#6715,#6716,#6717));
#2019=EDGE_LOOP('',(#6718,#6719,#6720,#6721));
#2020=EDGE_LOOP('',(#6722,#6723,#6724,#6725));
#2021=EDGE_LOOP('',(#6726));
#2022=EDGE_LOOP('',(#6727));
#2023=EDGE_LOOP('',(#6728,#6729,#6730,#6731));
#2024=EDGE_LOOP('',(#6732,#6733,#6734,#6735));
#2642=LINE('',#14523,#3288);
#2643=LINE('',#14525,#3289);
#2644=LINE('',#14527,#3290);
#2645=LINE('',#14528,#3291);
#2646=LINE('',#14531,#3292);
#2647=LINE('',#14533,#3293);
#2648=LINE('',#14534,#3294);
#2649=LINE('',#14537,#3295);
#2650=LINE('',#14539,#3296);
#2651=LINE('',#14540,#3297);
#2652=LINE('',#14543,#3298);
#2653=LINE('',#14545,#3299);
#2654=LINE('',#14546,#3300);
#2655=LINE('',#14549,#3301);
#2656=LINE('',#14551,#3302);
#2657=LINE('',#14552,#3303);
#2658=LINE('',#14554,#3304);
#2659=LINE('',#14555,#3305);
#2660=LINE('',#14567,#3306);
#2661=LINE('',#14571,#3307);
#2662=LINE('',#14575,#3308);
#2663=LINE('',#14582,#3309);
#2664=LINE('',#14584,#3310);
#3288=VECTOR('',#11378,1.);
#3289=VECTOR('',#11379,1.);
#3290=VECTOR('',#11380,1.);
#3291=VECTOR('',#11381,1.);
#3292=VECTOR('',#11384,1.);
#3293=VECTOR('',#11385,1.);
#3294=VECTOR('',#11386,1.);
#3295=VECTOR('',#11389,1.);
#3296=VECTOR('',#11390,1.);
#3297=VECTOR('',#11391,1.);
#3298=VECTOR('',#11394,1.);
#3299=VECTOR('',#11395,1.);
#3300=VECTOR('',#11396,1.);
#3301=VECTOR('',#11399,1.);
#3302=VECTOR('',#11400,1.);
#3303=VECTOR('',#11401,1.);
#3304=VECTOR('',#11404,1.);
#3305=VECTOR('',#11405,1.);
#3306=VECTOR('',#11422,0.625);
#3307=VECTOR('',#11427,0.65);
#3308=VECTOR('',#11432,0.635);
#3309=VECTOR('',#11441,0.41);
#3310=VECTOR('',#11444,0.4);
#3886=CIRCLE('',#9816,0.3933);
#3887=CIRCLE('',#9818,0.6);
#3888=CIRCLE('',#9820,0.65);
#3889=CIRCLE('',#9822,0.65);
#3890=CIRCLE('',#9824,0.62);
#3891=CIRCLE('',#9826,0.42);
#3892=CIRCLE('',#9828,0.3933);
#4386=VERTEX_POINT('',#14521);
#4387=VERTEX_POINT('',#14522);
#4388=VERTEX_POINT('',#14524);
#4389=VERTEX_POINT('',#14526);
#4390=VERTEX_POINT('',#14530);
#4391=VERTEX_POINT('',#14532);
#4392=VERTEX_POINT('',#14536);
#4393=VERTEX_POINT('',#14538);
#4394=VERTEX_POINT('',#14542);
#4395=VERTEX_POINT('',#14544);
#4396=VERTEX_POINT('',#14548);
#4397=VERTEX_POINT('',#14550);
#4398=VERTEX_POINT('',#14559);
#4399=VERTEX_POINT('',#14562);
#4400=VERTEX_POINT('',#14565);
#4401=VERTEX_POINT('',#14569);
#4402=VERTEX_POINT('',#14573);
#4403=VERTEX_POINT('',#14577);
#4404=VERTEX_POINT('',#14580);
#5236=EDGE_CURVE('',#4386,#4387,#2642,.T.);
#5237=EDGE_CURVE('',#4387,#4388,#2643,.T.);
#5238=EDGE_CURVE('',#4388,#4389,#2644,.T.);
#5239=EDGE_CURVE('',#4386,#4389,#2645,.T.);
#5240=EDGE_CURVE('',#4387,#4390,#2646,.T.);
#5241=EDGE_CURVE('',#4390,#4391,#2647,.T.);
#5242=EDGE_CURVE('',#4391,#4388,#2648,.T.);
#5243=EDGE_CURVE('',#4390,#4392,#2649,.T.);
#5244=EDGE_CURVE('',#4392,#4393,#2650,.T.);
#5245=EDGE_CURVE('',#4393,#4391,#2651,.T.);
#5246=EDGE_CURVE('',#4392,#4394,#2652,.T.);
#5247=EDGE_CURVE('',#4394,#4395,#2653,.T.);
#5248=EDGE_CURVE('',#4395,#4393,#2654,.T.);
#5249=EDGE_CURVE('',#4394,#4396,#2655,.T.);
#5250=EDGE_CURVE('',#4396,#4397,#2656,.T.);
#5251=EDGE_CURVE('',#4397,#4395,#2657,.T.);
#5252=EDGE_CURVE('',#4396,#4386,#2658,.T.);
#5253=EDGE_CURVE('',#4389,#4397,#2659,.T.);
#5254=EDGE_CURVE('',#4398,#4398,#3886,.T.);
#5255=EDGE_CURVE('',#4399,#4399,#3887,.T.);
#5256=EDGE_CURVE('',#4400,#4400,#3888,.T.);
#5257=EDGE_CURVE('',#4400,#4399,#2660,.T.);
#5258=EDGE_CURVE('',#4401,#4401,#3889,.T.);
#5259=EDGE_CURVE('',#4401,#4400,#2661,.T.);
#5260=EDGE_CURVE('',#4402,#4402,#3890,.T.);
#5261=EDGE_CURVE('',#4402,#4401,#2662,.T.);
#5262=EDGE_CURVE('',#4403,#4403,#3891,.T.);
#5263=EDGE_CURVE('',#4404,#4404,#3892,.F.);
#5264=EDGE_CURVE('',#4404,#4403,#2663,.T.);
#5265=EDGE_CURVE('',#4398,#4404,#2664,.T.);
#6676=ORIENTED_EDGE('',*,*,#5236,.T.);
#6677=ORIENTED_EDGE('',*,*,#5237,.T.);
#6678=ORIENTED_EDGE('',*,*,#5238,.T.);
#6679=ORIENTED_EDGE('',*,*,#5239,.F.);
#6680=ORIENTED_EDGE('',*,*,#5240,.T.);
#6681=ORIENTED_EDGE('',*,*,#5241,.T.);
#6682=ORIENTED_EDGE('',*,*,#5242,.T.);
#6683=ORIENTED_EDGE('',*,*,#5237,.F.);
#6684=ORIENTED_EDGE('',*,*,#5243,.T.);
#6685=ORIENTED_EDGE('',*,*,#5244,.T.);
#6686=ORIENTED_EDGE('',*,*,#5245,.T.);
#6687=ORIENTED_EDGE('',*,*,#5241,.F.);
#6688=ORIENTED_EDGE('',*,*,#5246,.T.);
#6689=ORIENTED_EDGE('',*,*,#5247,.T.);
#6690=ORIENTED_EDGE('',*,*,#5248,.T.);
#6691=ORIENTED_EDGE('',*,*,#5244,.F.);
#6692=ORIENTED_EDGE('',*,*,#5249,.T.);
#6693=ORIENTED_EDGE('',*,*,#5250,.T.);
#6694=ORIENTED_EDGE('',*,*,#5251,.T.);
#6695=ORIENTED_EDGE('',*,*,#5247,.F.);
#6696=ORIENTED_EDGE('',*,*,#5252,.T.);
#6697=ORIENTED_EDGE('',*,*,#5239,.T.);
#6698=ORIENTED_EDGE('',*,*,#5253,.T.);
#6699=ORIENTED_EDGE('',*,*,#5250,.F.);
#6700=ORIENTED_EDGE('',*,*,#5252,.F.);
#6701=ORIENTED_EDGE('',*,*,#5249,.F.);
#6702=ORIENTED_EDGE('',*,*,#5246,.F.);
#6703=ORIENTED_EDGE('',*,*,#5243,.F.);
#6704=ORIENTED_EDGE('',*,*,#5240,.F.);
#6705=ORIENTED_EDGE('',*,*,#5236,.F.);
#6706=ORIENTED_EDGE('',*,*,#5253,.F.);
#6707=ORIENTED_EDGE('',*,*,#5238,.F.);
#6708=ORIENTED_EDGE('',*,*,#5242,.F.);
#6709=ORIENTED_EDGE('',*,*,#5245,.F.);
#6710=ORIENTED_EDGE('',*,*,#5248,.F.);
#6711=ORIENTED_EDGE('',*,*,#5251,.F.);
#6712=ORIENTED_EDGE('',*,*,#5254,.F.);
#6713=ORIENTED_EDGE('',*,*,#5255,.F.);
#6714=ORIENTED_EDGE('',*,*,#5256,.F.);
#6715=ORIENTED_EDGE('',*,*,#5257,.T.);
#6716=ORIENTED_EDGE('',*,*,#5255,.T.);
#6717=ORIENTED_EDGE('',*,*,#5257,.F.);
#6718=ORIENTED_EDGE('',*,*,#5258,.F.);
#6719=ORIENTED_EDGE('',*,*,#5259,.T.);
#6720=ORIENTED_EDGE('',*,*,#5256,.T.);
#6721=ORIENTED_EDGE('',*,*,#5259,.F.);
#6722=ORIENTED_EDGE('',*,*,#5260,.F.);
#6723=ORIENTED_EDGE('',*,*,#5261,.T.);
#6724=ORIENTED_EDGE('',*,*,#5258,.T.);
#6725=ORIENTED_EDGE('',*,*,#5261,.F.);
#6726=ORIENTED_EDGE('',*,*,#5260,.T.);
#6727=ORIENTED_EDGE('',*,*,#5262,.F.);
#6728=ORIENTED_EDGE('',*,*,#5263,.F.);
#6729=ORIENTED_EDGE('',*,*,#5264,.T.);
#6730=ORIENTED_EDGE('',*,*,#5262,.T.);
#6731=ORIENTED_EDGE('',*,*,#5264,.F.);
#6732=ORIENTED_EDGE('',*,*,#5254,.T.);
#6733=ORIENTED_EDGE('',*,*,#5265,.T.);
#6734=ORIENTED_EDGE('',*,*,#5263,.T.);
#6735=ORIENTED_EDGE('',*,*,#5265,.F.);
#8265=CYLINDRICAL_SURFACE('',#9821,0.65);
#8266=CYLINDRICAL_SURFACE('',#9829,0.3933);
#8516=ADVANCED_FACE('',(#1378),#987,.F.);
#8517=ADVANCED_FACE('',(#1379),#988,.F.);
#8518=ADVANCED_FACE('',(#1380),#989,.F.);
#8519=ADVANCED_FACE('',(#1381),#990,.F.);
#8520=ADVANCED_FACE('',(#1382),#991,.F.);
#8521=ADVANCED_FACE('',(#1383),#992,.F.);
#8522=ADVANCED_FACE('',(#1384),#993,.F.);
#8523=ADVANCED_FACE('',(#1385),#994,.F.);
#8524=ADVANCED_FACE('',(#1386),#995,.F.);
#8525=ADVANCED_FACE('',(#1387),#996,.T.);
#8526=ADVANCED_FACE('',(#1388),#13,.T.);
#8527=ADVANCED_FACE('',(#1389),#8265,.T.);
#8528=ADVANCED_FACE('',(#1390),#14,.T.);
#8529=ADVANCED_FACE('',(#1391,#807),#997,.T.);
#8530=ADVANCED_FACE('',(#1392),#15,.T.);
#8531=ADVANCED_FACE('',(#1393),#8266,.T.);
#8892=CLOSED_SHELL('',(#8516,#8517,#8518,#8519,#8520,#8521,#8522,#8523));
#8893=CLOSED_SHELL('',(#8524,#8525,#8526,#8527,#8528,#8529,#8530,#8531));
#9806=AXIS2_PLACEMENT_3D('',#14519,#11374,#11375);
#9807=AXIS2_PLACEMENT_3D('',#14520,#11376,#11377);
#9808=AXIS2_PLACEMENT_3D('',#14529,#11382,#11383);
#9809=AXIS2_PLACEMENT_3D('',#14535,#11387,#11388);
#9810=AXIS2_PLACEMENT_3D('',#14541,#11392,#11393);
#9811=AXIS2_PLACEMENT_3D('',#14547,#11397,#11398);
#9812=AXIS2_PLACEMENT_3D('',#14553,#11402,#11403);
#9813=AXIS2_PLACEMENT_3D('',#14556,#11406,#11407);
#9814=AXIS2_PLACEMENT_3D('',#14557,#11408,#11409);
#9815=AXIS2_PLACEMENT_3D('',#14558,#11410,#11411);
#9816=AXIS2_PLACEMENT_3D('',#14560,#11412,#11413);
#9817=AXIS2_PLACEMENT_3D('',#14561,#11414,#11415);
#9818=AXIS2_PLACEMENT_3D('',#14563,#11416,#11417);
#9819=AXIS2_PLACEMENT_3D('',#14564,#11418,#11419);
#9820=AXIS2_PLACEMENT_3D('',#14566,#11420,#11421);
#9821=AXIS2_PLACEMENT_3D('',#14568,#11423,#11424);
#9822=AXIS2_PLACEMENT_3D('',#14570,#11425,#11426);
#9823=AXIS2_PLACEMENT_3D('',#14572,#11428,#11429);
#9824=AXIS2_PLACEMENT_3D('',#14574,#11430,#11431);
#9825=AXIS2_PLACEMENT_3D('',#14576,#11433,#11434);
#9826=AXIS2_PLACEMENT_3D('',#14578,#11435,#11436);
#9827=AXIS2_PLACEMENT_3D('',#14579,#11437,#11438);
#9828=AXIS2_PLACEMENT_3D('',#14581,#11439,#11440);
#9829=AXIS2_PLACEMENT_3D('',#14583,#11442,#11443);
#11374=DIRECTION('axis',(0.,0.,1.));
#11375=DIRECTION('refdir',(1.,0.,0.));
#11376=DIRECTION('center_axis',(0.866025403784439,0.,-0.5));
#11377=DIRECTION('ref_axis',(0.5,0.,0.866025403784439));
#11378=DIRECTION('',(-0.5,0.,-0.866025403784439));
#11379=DIRECTION('',(0.,-1.,0.));
#11380=DIRECTION('',(0.5,0.,0.866025403784439));
#11381=DIRECTION('',(0.,-1.,0.));
#11382=DIRECTION('center_axis',(1.60246890531964E-16,0.,-1.));
#11383=DIRECTION('ref_axis',(1.,0.,1.60246890531964E-16));
#11384=DIRECTION('',(-1.,0.,-1.60246890531964E-16));
#11385=DIRECTION('',(0.,-1.,0.));
#11386=DIRECTION('',(1.,0.,1.60246890531964E-16));
#11387=DIRECTION('center_axis',(-0.866025403784439,0.,-0.5));
#11388=DIRECTION('ref_axis',(0.5,0.,-0.866025403784439));
#11389=DIRECTION('',(-0.5,0.,0.866025403784439));
#11390=DIRECTION('',(0.,-1.,0.));
#11391=DIRECTION('',(0.5,0.,-0.866025403784439));
#11392=DIRECTION('center_axis',(-0.866025403784439,0.,0.5));
#11393=DIRECTION('ref_axis',(-0.5,0.,-0.866025403784439));
#11394=DIRECTION('',(0.5,0.,0.866025403784439));
#11395=DIRECTION('',(0.,-1.,0.));
#11396=DIRECTION('',(-0.5,0.,-0.866025403784439));
#11397=DIRECTION('center_axis',(-1.60246890531964E-16,0.,1.));
#11398=DIRECTION('ref_axis',(-1.,0.,-1.60246890531964E-16));
#11399=DIRECTION('',(1.,0.,1.60246890531964E-16));
#11400=DIRECTION('',(0.,-1.,0.));
#11401=DIRECTION('',(-1.,0.,-1.60246890531964E-16));
#11402=DIRECTION('center_axis',(0.866025403784439,0.,0.5));
#11403=DIRECTION('ref_axis',(-0.5,0.,0.866025403784439));
#11404=DIRECTION('',(0.5,0.,-0.866025403784439));
#11405=DIRECTION('',(-0.5,0.,0.866025403784439));
#11406=DIRECTION('center_axis',(0.,1.,0.));
#11407=DIRECTION('ref_axis',(1.,0.,0.));
#11408=DIRECTION('center_axis',(0.,-1.,0.));
#11409=DIRECTION('ref_axis',(0.,0.,-1.));
#11410=DIRECTION('center_axis',(0.,1.,0.));
#11411=DIRECTION('ref_axis',(1.,0.,0.));
#11412=DIRECTION('center_axis',(0.,1.,0.));
#11413=DIRECTION('ref_axis',(1.,0.,0.));
#11414=DIRECTION('center_axis',(0.,1.,0.));
#11415=DIRECTION('ref_axis',(0.,0.,1.));
#11416=DIRECTION('center_axis',(0.,-1.,0.));
#11417=DIRECTION('ref_axis',(1.,0.,0.));
#11418=DIRECTION('center_axis',(0.,-1.,0.));
#11419=DIRECTION('ref_axis',(1.,0.,0.));
#11420=DIRECTION('center_axis',(0.,-1.,0.));
#11421=DIRECTION('ref_axis',(1.,0.,0.));
#11422=DIRECTION('',(0.707106781186548,0.707106781186547,8.65956056235493E-17));
#11423=DIRECTION('center_axis',(0.,-1.,0.));
#11424=DIRECTION('ref_axis',(1.,0.,0.));
#11425=DIRECTION('center_axis',(0.,-1.,0.));
#11426=DIRECTION('ref_axis',(1.,0.,0.));
#11427=DIRECTION('',(0.,1.,0.));
#11428=DIRECTION('center_axis',(0.,1.,0.));
#11429=DIRECTION('ref_axis',(1.,0.,0.));
#11430=DIRECTION('center_axis',(0.,-1.,0.));
#11431=DIRECTION('ref_axis',(1.,0.,0.));
#11432=DIRECTION('',(-0.707106781186548,0.707106781186547,-8.65956056235494E-17));
#11433=DIRECTION('center_axis',(0.,-1.,0.));
#11434=DIRECTION('ref_axis',(0.,0.,-1.));
#11435=DIRECTION('center_axis',(0.,-1.,0.));
#11436=DIRECTION('ref_axis',(1.,0.,0.));
#11437=DIRECTION('center_axis',(0.,1.,0.));
#11438=DIRECTION('ref_axis',(1.,0.,0.));
#11439=DIRECTION('center_axis',(0.,1.,0.));
#11440=DIRECTION('ref_axis',(1.,0.,0.));
#11441=DIRECTION('',(-0.447213595499958,0.894427190999916,-5.47678698264203E-17));
#11442=DIRECTION('center_axis',(0.,-1.,0.));
#11443=DIRECTION('ref_axis',(1.,0.,0.));
#11444=DIRECTION('',(0.,1.,0.));
#14519=CARTESIAN_POINT('',(0.,0.,0.));
#14520=CARTESIAN_POINT('Origin',(0.173205080756888,-0.8,-0.3));
#14521=CARTESIAN_POINT('',(0.346410161513775,-0.8,0.));
#14522=CARTESIAN_POINT('',(0.173205080756888,-0.8,-0.3));
#14523=CARTESIAN_POINT('',(0.346410161513775,-0.8,0.));
#14524=CARTESIAN_POINT('',(0.173205080756888,-1.28,-0.3));
#14525=CARTESIAN_POINT('',(0.173205080756888,-0.8,-0.3));
#14526=CARTESIAN_POINT('',(0.346410161513775,-1.28,0.));
#14527=CARTESIAN_POINT('',(0.346410161513775,-1.28,0.));
#14528=CARTESIAN_POINT('',(0.346410161513775,-0.8,0.));
#14529=CARTESIAN_POINT('Origin',(-0.173205080756888,-0.8,-0.3));
#14530=CARTESIAN_POINT('',(-0.173205080756888,-0.8,-0.3));
#14531=CARTESIAN_POINT('',(0.173205080756888,-0.8,-0.3));
#14532=CARTESIAN_POINT('',(-0.173205080756888,-1.28,-0.3));
#14533=CARTESIAN_POINT('',(-0.173205080756888,-0.8,-0.3));
#14534=CARTESIAN_POINT('',(0.173205080756888,-1.28,-0.3));
#14535=CARTESIAN_POINT('Origin',(-0.346410161513775,-0.8,-5.55111512312578E-17));
#14536=CARTESIAN_POINT('',(-0.346410161513775,-0.8,-4.24230095489963E-17));
#14537=CARTESIAN_POINT('',(-0.173205080756888,-0.8,-0.3));
#14538=CARTESIAN_POINT('',(-0.346410161513775,-1.28,-5.55111512312578E-17));
#14539=CARTESIAN_POINT('',(-0.346410161513775,-0.8,-4.24230095489963E-17));
#14540=CARTESIAN_POINT('',(-0.173205080756888,-1.28,-0.3));
#14541=CARTESIAN_POINT('Origin',(-0.173205080756888,-0.8,0.3));
#14542=CARTESIAN_POINT('',(-0.173205080756888,-0.8,0.3));
#14543=CARTESIAN_POINT('',(-0.346410161513775,-0.8,-4.24230095489963E-17));
#14544=CARTESIAN_POINT('',(-0.173205080756888,-1.28,0.3));
#14545=CARTESIAN_POINT('',(-0.173205080756888,-0.8,0.3));
#14546=CARTESIAN_POINT('',(-0.346410161513775,-1.28,-4.24230095489963E-17));
#14547=CARTESIAN_POINT('Origin',(0.173205080756888,-0.8,0.3));
#14548=CARTESIAN_POINT('',(0.173205080756888,-0.8,0.3));
#14549=CARTESIAN_POINT('',(-0.173205080756888,-0.8,0.3));
#14550=CARTESIAN_POINT('',(0.173205080756888,-1.28,0.3));
#14551=CARTESIAN_POINT('',(0.173205080756888,-0.8,0.3));
#14552=CARTESIAN_POINT('',(-0.173205080756888,-1.28,0.3));
#14553=CARTESIAN_POINT('Origin',(0.346410161513775,-0.8,0.));
#14554=CARTESIAN_POINT('',(0.173205080756888,-0.8,0.3));
#14555=CARTESIAN_POINT('',(0.173205080756888,-1.28,0.3));
#14556=CARTESIAN_POINT('Origin',(0.,-0.8,-5.55111512312578E-17));
#14557=CARTESIAN_POINT('Origin',(0.,-1.28,-5.55111512312578E-17));
#14558=CARTESIAN_POINT('Origin',(0.,-2.5,0.));
#14559=CARTESIAN_POINT('',(-0.3933,-2.5,4.81653586104654E-17));
#14560=CARTESIAN_POINT('Origin',(0.,-2.5,0.));
#14561=CARTESIAN_POINT('Origin',(0.6,0.8,0.));
#14562=CARTESIAN_POINT('',(-0.6,0.8,-7.34788079488412E-17));
#14563=CARTESIAN_POINT('Origin',(0.,0.8,0.));
#14564=CARTESIAN_POINT('Origin',(0.,0.775,0.));
#14565=CARTESIAN_POINT('',(-0.65,0.75,-7.9602041944578E-17));
#14566=CARTESIAN_POINT('Origin',(0.,0.75,0.));
#14567=CARTESIAN_POINT('',(-0.625,0.775,-7.65404249467096E-17));
#14568=CARTESIAN_POINT('Origin',(0.,0.39,0.));
#14569=CARTESIAN_POINT('',(-0.65,0.0299999999999998,-7.9602041944578E-17));
#14570=CARTESIAN_POINT('Origin',(0.,0.0299999999999998,0.));
#14571=CARTESIAN_POINT('',(-0.65,0.39,-7.9602041944578E-17));
#14572=CARTESIAN_POINT('Origin',(0.,0.0150000000000001,0.));
#14573=CARTESIAN_POINT('',(-0.62,5.89805981832114E-17,-7.59281015471359E-17));
#14574=CARTESIAN_POINT('Origin',(0.,0.,0.));
#14575=CARTESIAN_POINT('',(-0.635,0.0150000000000001,-7.77650717458569E-17));
#14576=CARTESIAN_POINT('Origin',(0.42,0.,0.));
#14577=CARTESIAN_POINT('',(-0.42,-3.46944695195361E-18,-5.14351655641888E-17));
#14578=CARTESIAN_POINT('Origin',(0.,0.,0.));
#14579=CARTESIAN_POINT('Origin',(0.,-0.02,0.));
#14580=CARTESIAN_POINT('',(-0.3933,-0.0534000000000001,4.81653586104654E-17));
#14581=CARTESIAN_POINT('Origin',(0.,-0.0534000000000001,0.));
#14582=CARTESIAN_POINT('',(-0.41,-0.02,-5.02105187650415E-17));
#14583=CARTESIAN_POINT('Origin',(0.,-1.48,0.));
#14584=CARTESIAN_POINT('',(-0.3933,-1.48,-4.81653586104654E-17));
#16810=UNCERTAINTY_MEASURE_WITH_UNIT(LENGTH_MEASURE(0.001),#16912,
'DISTANCE_ACCURACY_VALUE',
'Maximum model space distance between geometric entities at asserted c
onnectivities');
#16852=UNCERTAINTY_MEASURE_WITH_UNIT(LENGTH_MEASURE(0.001),#16912,
'DISTANCE_ACCURACY_VALUE',
'Maximum model space distance between geometric entities at asserted c
onnectivities');
#16869=(
GEOMETRIC_REPRESENTATION_CONTEXT(3)
GLOBAL_UNCERTAINTY_ASSIGNED_CONTEXT((#16810))
GLOBAL_UNIT_ASSIGNED_CONTEXT((#16912,#16914,#16915))
REPRESENTATION_CONTEXT('','3D')
);
#16911=(
GEOMETRIC_REPRESENTATION_CONTEXT(3)
GLOBAL_UNCERTAINTY_ASSIGNED_CONTEXT((#16852))
GLOBAL_UNIT_ASSIGNED_CONTEXT((#16912,#16914,#16915))
REPRESENTATION_CONTEXT('','3D')
);
#16912=(
LENGTH_UNIT()
NAMED_UNIT(*)
SI_UNIT(.CENTI.,.METRE.)
);
#16914=(
NAMED_UNIT(*)
PLANE_ANGLE_UNIT()
SI_UNIT($,.RADIAN.)
);
#16915=(
NAMED_UNIT(*)
SI_UNIT($,.STERADIAN.)
SOLID_ANGLE_UNIT()
);
#16932=SHAPE_DEFINITION_REPRESENTATION(#16992,#17140);
#16992=PRODUCT_DEFINITION_SHAPE('',$,#17199);
#17140=SHAPE_REPRESENTATION('',(#9806),#16869);
#17182=PRODUCT_DEFINITION_CONTEXT('part definition',#17358,'design');
#17199=PRODUCT_DEFINITION('M8x25 Bolt','M8x25 Bolt',#17257,#17182);
#17257=PRODUCT_DEFINITION_FORMATION('',$,#17376);
#17358=APPLICATION_CONTEXT(
'Core Data for Automotive Mechanical Design Process');
#17359=PRODUCT_CONTEXT('part definition',#17358,'mechanical');
#17376=PRODUCT('M8x25 Bolt','M8x25 Bolt','M8x25 Bolt',(#17359));
#17488=COLOUR_RGB('Black',0.12,0.14,0.17);
#17489=FILL_AREA_STYLE_COLOUR('',#17488);
#17490=FILL_AREA_STYLE('',(#17489));
#17491=SURFACE_STYLE_FILL_AREA(#17490);
#17492=SURFACE_SIDE_STYLE('',(#17491));
#17493=SURFACE_STYLE_USAGE(.BOTH.,#17492);
#17494=PRESENTATION_STYLE_ASSIGNMENT((#17493));
ENDSEC;
END-ISO-10303-21;
